ISO-10303-21;
HEADER;
/* Generated by software containing ST-Developer
 * from STEP Tools, Inc. (www.steptools.com) 
 */

FILE_DESCRIPTION(
/* description */ (''),
/* implementation_level */ '2;1');

FILE_NAME(
/* name */ 'Ring.step',
/* time_stamp */ '2026-10-23T17:22:31+06:00',
/* author */ (''),
/* organization */ (''),
/* preprocessor_version */ 'ST-DEVELOPER v20.2',
/* originating_system */ 'Autodesk Translation Framework v15.15.0.0',
/* authorisation */ '');

FILE_SCHEMA (('AUTOMOTIVE_DESIGN { 1 0 10303 214 3 1 1 }'));
ENDSEC;

DATA;
#10=MECHANICAL_DESIGN_GEOMETRIC_PRESENTATION_REPRESENTATION('',(#86),#7315);
#66=SHAPE_REPRESENTATION_RELATIONSHIP('SRR','None',#7362,#76);
#76=ADVANCED_BREP_SHAPE_REPRESENTATION('',(#96),#7314);
#86=STYLED_ITEM('',(#7431),#96);
#96=MANIFOLD_SOLID_BREP('Ring',#3223);
#387=LINE('',#7272,#547);
#388=LINE('',#7278,#548);
#547=VECTOR('',#4628,3.72286361298787);
#548=VECTOR('',#4635,5.22286361298787);
#687=CYLINDRICAL_SURFACE('',#3706,3.72286361298787);
#688=CYLINDRICAL_SURFACE('',#3709,5.22286361298787);
#698=FACE_BOUND('',#1100,.T.);
#699=FACE_BOUND('',#1102,.T.);
#726=PLANE('',#3712);
#727=PLANE('',#3713);
#906=FACE_OUTER_BOUND('',#1097,.T.);
#907=FACE_OUTER_BOUND('',#1098,.T.);
#908=FACE_OUTER_BOUND('',#1099,.T.);
#909=FACE_OUTER_BOUND('',#1101,.T.);
#1097=EDGE_LOOP('',(#3016,#3017,#3018,#3019));
#1098=EDGE_LOOP('',(#3020,#3021,#3022,#3023));
#1099=EDGE_LOOP('',(#3024));
#1100=EDGE_LOOP('',(#3025));
#1101=EDGE_LOOP('',(#3026));
#1102=EDGE_LOOP('',(#3027));
#1285=CIRCLE('',#3707,3.72286361298787);
#1286=CIRCLE('',#3708,3.72286361298787);
#1287=CIRCLE('',#3710,5.22286361298787);
#1288=CIRCLE('',#3711,5.22286361298787);
#1602=VERTEX_POINT('',#7269);
#1603=VERTEX_POINT('',#7271);
#1604=VERTEX_POINT('',#7275);
#1605=VERTEX_POINT('',#7277);
#2074=EDGE_CURVE('',#1602,#1602,#1285,.T.);
#2075=EDGE_CURVE('',#1602,#1603,#387,.T.);
#2076=EDGE_CURVE('',#1603,#1603,#1286,.T.);
#2077=EDGE_CURVE('',#1604,#1604,#1287,.T.);
#2078=EDGE_CURVE('',#1604,#1605,#388,.T.);
#2079=EDGE_CURVE('',#1605,#1605,#1288,.T.);
#3016=ORIENTED_EDGE('',*,*,#2074,.F.);
#3017=ORIENTED_EDGE('',*,*,#2075,.T.);
#3018=ORIENTED_EDGE('',*,*,#2076,.T.);
#3019=ORIENTED_EDGE('',*,*,#2075,.F.);
#3020=ORIENTED_EDGE('',*,*,#2077,.F.);
#3021=ORIENTED_EDGE('',*,*,#2078,.T.);
#3022=ORIENTED_EDGE('',*,*,#2079,.T.);
#3023=ORIENTED_EDGE('',*,*,#2078,.F.);
#3024=ORIENTED_EDGE('',*,*,#2077,.T.);
#3025=ORIENTED_EDGE('',*,*,#2074,.T.);
#3026=ORIENTED_EDGE('',*,*,#2079,.F.);
#3027=ORIENTED_EDGE('',*,*,#2076,.F.);
#3210=ADVANCED_FACE('',(#906),#687,.F.);
#3211=ADVANCED_FACE('',(#907),#688,.T.);
#3212=ADVANCED_FACE('',(#908,#698),#726,.T.);
#3213=ADVANCED_FACE('',(#909,#699),#727,.F.);
#3223=CLOSED_SHELL('',(#3210,#3211,#3212,#3213));
#3705=AXIS2_PLACEMENT_3D('',#7267,#4622,#4623);
#3706=AXIS2_PLACEMENT_3D('',#7268,#4624,#4625);
#3707=AXIS2_PLACEMENT_3D('',#7270,#4626,#4627);
#3708=AXIS2_PLACEMENT_3D('',#7273,#4629,#4630);
#3709=AXIS2_PLACEMENT_3D('',#7274,#4631,#4632);
#3710=AXIS2_PLACEMENT_3D('',#7276,#4633,#4634);
#3711=AXIS2_PLACEMENT_3D('',#7279,#4636,#4637);
#3712=AXIS2_PLACEMENT_3D('',#7280,#4638,#4639);
#3713=AXIS2_PLACEMENT_3D('',#7281,#4640,#4641);
#4622=DIRECTION('axis',(0.,0.,1.));
#4623=DIRECTION('refdir',(1.,0.,0.));
#4624=DIRECTION('center_axis',(-1.,0.,0.));
#4625=DIRECTION('ref_axis',(0.,-1.,0.));
#4626=DIRECTION('center_axis',(1.,0.,0.));
#4627=DIRECTION('ref_axis',(0.,-1.,0.));
#4628=DIRECTION('',(1.,0.,0.));
#4629=DIRECTION('center_axis',(1.,0.,0.));
#4630=DIRECTION('ref_axis',(0.,-1.,0.));
#4631=DIRECTION('center_axis',(-1.,0.,0.));
#4632=DIRECTION('ref_axis',(0.,-1.,0.));
#4633=DIRECTION('center_axis',(-1.,0.,0.));
#4634=DIRECTION('ref_axis',(0.,-1.,0.));
#4635=DIRECTION('',(1.,0.,0.));
#4636=DIRECTION('center_axis',(-1.,0.,0.));
#4637=DIRECTION('ref_axis',(0.,-1.,0.));
#4638=DIRECTION('center_axis',(-1.,0.,0.));
#4639=DIRECTION('ref_axis',(0.,-1.,0.));
#4640=DIRECTION('center_axis',(-1.,0.,0.));
#4641=DIRECTION('ref_axis',(0.,-1.,0.));
#7267=CARTESIAN_POINT('',(0.,0.,0.));
#7268=CARTESIAN_POINT('Origin',(21.2197085942866,0.,0.));
#7269=CARTESIAN_POINT('',(20.2197085942866,3.72286361298787,-4.55919300730774E-16));
#7270=CARTESIAN_POINT('Origin',(20.2197085942866,0.,0.));
#7271=CARTESIAN_POINT('',(21.2197085942866,3.72286361298787,-4.55919300730774E-16));
#7272=CARTESIAN_POINT('',(21.2197085942866,3.72286361298787,-4.55919300730774E-16));
#7273=CARTESIAN_POINT('Origin',(21.2197085942866,0.,0.));
#7274=CARTESIAN_POINT('Origin',(21.2197085942866,0.,0.));
#7275=CARTESIAN_POINT('',(20.2197085942866,5.22286361298787,-6.39616320602877E-16));
#7276=CARTESIAN_POINT('Origin',(20.2197085942866,0.,0.));
#7277=CARTESIAN_POINT('',(21.2197085942866,5.22286361298787,-6.39616320602877E-16));
#7278=CARTESIAN_POINT('',(21.2197085942866,5.22286361298787,-6.39616320602877E-16));
#7279=CARTESIAN_POINT('Origin',(21.2197085942866,0.,0.));
#7280=CARTESIAN_POINT('Origin',(20.2197085942866,0.,0.));
#7281=CARTESIAN_POINT('Origin',(21.2197085942866,0.,0.));
#7302=UNCERTAINTY_MEASURE_WITH_UNIT(LENGTH_MEASURE(0.01),#7316,
'DISTANCE_ACCURACY_VALUE',
'Maximum model space distance between geometric entities at asserted c
onnectivities');
#7303=UNCERTAINTY_MEASURE_WITH_UNIT(LENGTH_MEASURE(0.01),#7316,
'DISTANCE_ACCURACY_VALUE',
'Maximum model space distance between geometric entities at asserted c
onnectivities');
#7314=(
GEOMETRIC_REPRESENTATION_CONTEXT(3)
GLOBAL_UNCERTAINTY_ASSIGNED_CONTEXT((#7302))
GLOBAL_UNIT_ASSIGNED_CONTEXT((#7316,#7318,#7319))
REPRESENTATION_CONTEXT('','3D')
);
#7315=(
GEOMETRIC_REPRESENTATION_CONTEXT(3)
GLOBAL_UNCERTAINTY_ASSIGNED_CONTEXT((#7303))
GLOBAL_UNIT_ASSIGNED_CONTEXT((#7316,#7318,#7319))
REPRESENTATION_CONTEXT('','3D')
);
#7316=(
LENGTH_UNIT()
NAMED_UNIT(*)
SI_UNIT(.MILLI.,.METRE.)
);
#7318=(
NAMED_UNIT(*)
PLANE_ANGLE_UNIT()
SI_UNIT($,.RADIAN.)
);
#7319=(
NAMED_UNIT(*)
SI_UNIT($,.STERADIAN.)
SOLID_ANGLE_UNIT()
);
#7330=SHAPE_DEFINITION_REPRESENTATION(#7341,#7362);
#7341=PRODUCT_DEFINITION_SHAPE('',$,#7374);
#7362=SHAPE_REPRESENTATION('',(#3705),#7314);
#7363=PRODUCT_DEFINITION_CONTEXT('part definition',#7398,'design');
#7374=PRODUCT_DEFINITION('Ring','Ring',#7385,#7363);
#7385=PRODUCT_DEFINITION_FORMATION('',$,#7410);
#7398=APPLICATION_CONTEXT(
'Core Data for Automotive Mechanical Design Process');
#7399=PRODUCT_CONTEXT('part definition',#7398,'mechanical');
#7410=PRODUCT('Ring','Ring',$,(#7399));
#7425=COLOUR_RGB('Light Blue',0.38,0.62,0.78);
#7426=FILL_AREA_STYLE_COLOUR('',#7425);
#7427=FILL_AREA_STYLE('',(#7426));
#7428=SURFACE_STYLE_FILL_AREA(#7427);
#7429=SURFACE_SIDE_STYLE('',(#7428));
#7430=SURFACE_STYLE_USAGE(.BOTH.,#7429);
#7431=PRESENTATION_STYLE_ASSIGNMENT((#7430));
ENDSEC;
END-ISO-10303-21;
